ISO-10303-21;
HEADER;
/* Generated by software containing ST-Developer
 * from STEP Tools, Inc. (www.steptools.com) 
 */

FILE_DESCRIPTION(
/* description */ ('PAT-091'),
/* implementation_level */ '2;1');

FILE_NAME(
/* name */ 'Axle end keeper (1).step',
/* time_stamp */ '2026-10-27T15:34:44-07:00',
/* author */ (''),
/* organization */ (''),
/* preprocessor_version */ 'ST-DEVELOPER v20.2',
/* originating_system */ 'Autodesk Translation Framework v15.17.0.0',
/* authorisation */ '');

FILE_SCHEMA (('AUTOMOTIVE_DESIGN { 1 0 10303 214 3 1 1 }'));
ENDSEC;

DATA;
#10=MECHANICAL_DESIGN_GEOMETRIC_PRESENTATION_REPRESENTATION('',(#984),#25100);
#764=SHAPE_REPRESENTATION_RELATIONSHIP('SRR','None',#25525,#874);
#874=ADVANCED_BREP_SHAPE_REPRESENTATION('',(#1108),#24995);
#984=STYLED_ITEM('',(#26191),#1108);
#1108=MANIFOLD_SOLID_BREP('Body1',#13261);
#1325=FACE_BOUND('',#3120,.T.);
#1326=FACE_BOUND('',#3122,.T.);
#1700=PLANE('',#14865);
#1701=PLANE('',#14866);
#2189=FACE_OUTER_BOUND('',#3117,.T.);
#2190=FACE_OUTER_BOUND('',#3118,.T.);
#2191=FACE_OUTER_BOUND('',#3119,.T.);
#2192=FACE_OUTER_BOUND('',#3121,.T.);
#3117=EDGE_LOOP('',(#9536,#9537,#9538,#9539));
#3118=EDGE_LOOP('',(#9540,#9541,#9542,#9543));
#3119=EDGE_LOOP('',(#9544));
#3120=EDGE_LOOP('',(#9545));
#3121=EDGE_LOOP('',(#9546));
#3122=EDGE_LOOP('',(#9547));
#4274=LINE('',#21590,#5014);
#4275=LINE('',#21596,#5015);
#5014=VECTOR('',#17170,0.225);
#5015=VECTOR('',#17177,1.);
#5736=CIRCLE('',#14860,0.225);
#5737=CIRCLE('',#14861,0.225);
#5738=CIRCLE('',#14863,1.);
#5739=CIRCLE('',#14864,1.);
#6571=VERTEX_POINT('',#21587);
#6572=VERTEX_POINT('',#21589);
#6573=VERTEX_POINT('',#21593);
#6574=VERTEX_POINT('',#21595);
#7703=EDGE_CURVE('',#6571,#6571,#5736,.T.);
#7704=EDGE_CURVE('',#6571,#6572,#4274,.T.);
#7705=EDGE_CURVE('',#6572,#6572,#5737,.T.);
#7706=EDGE_CURVE('',#6573,#6573,#5738,.T.);
#7707=EDGE_CURVE('',#6573,#6574,#4275,.T.);
#7708=EDGE_CURVE('',#6574,#6574,#5739,.T.);
#9536=ORIENTED_EDGE('',*,*,#7703,.F.);
#9537=ORIENTED_EDGE('',*,*,#7704,.T.);
#9538=ORIENTED_EDGE('',*,*,#7705,.T.);
#9539=ORIENTED_EDGE('',*,*,#7704,.F.);
#9540=ORIENTED_EDGE('',*,*,#7706,.F.);
#9541=ORIENTED_EDGE('',*,*,#7707,.T.);
#9542=ORIENTED_EDGE('',*,*,#7708,.T.);
#9543=ORIENTED_EDGE('',*,*,#7707,.F.);
#9544=ORIENTED_EDGE('',*,*,#7706,.T.);
#9545=ORIENTED_EDGE('',*,*,#7703,.T.);
#9546=ORIENTED_EDGE('',*,*,#7708,.F.);
#9547=ORIENTED_EDGE('',*,*,#7705,.F.);
#12140=CYLINDRICAL_SURFACE('',#14859,0.225);
#12141=CYLINDRICAL_SURFACE('',#14862,1.);
#12556=ADVANCED_FACE('',(#2189),#12140,.F.);
#12557=ADVANCED_FACE('',(#2190),#12141,.T.);
#12558=ADVANCED_FACE('',(#2191,#1325),#1700,.T.);
#12559=ADVANCED_FACE('',(#2192,#1326),#1701,.F.);
#13261=CLOSED_SHELL('',(#12556,#12557,#12558,#12559));
#14858=AXIS2_PLACEMENT_3D('',#21585,#17164,#17165);
#14859=AXIS2_PLACEMENT_3D('',#21586,#17166,#17167);
#14860=AXIS2_PLACEMENT_3D('',#21588,#17168,#17169);
#14861=AXIS2_PLACEMENT_3D('',#21591,#17171,#17172);
#14862=AXIS2_PLACEMENT_3D('',#21592,#17173,#17174);
#14863=AXIS2_PLACEMENT_3D('',#21594,#17175,#17176);
#14864=AXIS2_PLACEMENT_3D('',#21597,#17178,#17179);
#14865=AXIS2_PLACEMENT_3D('',#21598,#17180,#17181);
#14866=AXIS2_PLACEMENT_3D('',#21599,#17182,#17183);
#17164=DIRECTION('axis',(0.,0.,1.));
#17165=DIRECTION('refdir',(1.,0.,0.));
#17166=DIRECTION('center_axis',(0.,1.,0.));
#17167=DIRECTION('ref_axis',(1.,0.,0.));
#17168=DIRECTION('center_axis',(0.,-1.,0.));
#17169=DIRECTION('ref_axis',(1.,0.,0.));
#17170=DIRECTION('',(0.,-1.,0.));
#17171=DIRECTION('center_axis',(0.,-1.,0.));
#17172=DIRECTION('ref_axis',(1.,0.,0.));
#17173=DIRECTION('center_axis',(0.,1.,0.));
#17174=DIRECTION('ref_axis',(1.,0.,0.));
#17175=DIRECTION('center_axis',(0.,1.,0.));
#17176=DIRECTION('ref_axis',(1.,0.,0.));
#17177=DIRECTION('',(0.,-1.,0.));
#17178=DIRECTION('center_axis',(0.,1.,0.));
#17179=DIRECTION('ref_axis',(1.,0.,0.));
#17180=DIRECTION('center_axis',(0.,1.,0.));
#17181=DIRECTION('ref_axis',(1.,0.,0.));
#17182=DIRECTION('center_axis',(0.,1.,0.));
#17183=DIRECTION('ref_axis',(1.,0.,0.));
#21585=CARTESIAN_POINT('',(0.,0.,0.));
#21586=CARTESIAN_POINT('Origin',(0.,6.5,3.));
#21587=CARTESIAN_POINT('',(-0.225,6.7,3.));
#21588=CARTESIAN_POINT('Origin',(0.,6.7,3.));
#21589=CARTESIAN_POINT('',(-0.225,6.5,3.));
#21590=CARTESIAN_POINT('',(-0.225,6.5,3.));
#21591=CARTESIAN_POINT('Origin',(0.,6.5,3.));
#21592=CARTESIAN_POINT('Origin',(0.,6.5,3.));
#21593=CARTESIAN_POINT('',(-1.,6.7,3.));
#21594=CARTESIAN_POINT('Origin',(0.,6.7,3.));
#21595=CARTESIAN_POINT('',(-1.,6.5,3.));
#21596=CARTESIAN_POINT('',(-1.,6.5,3.));
#21597=CARTESIAN_POINT('Origin',(0.,6.5,3.));
#21598=CARTESIAN_POINT('Origin',(0.,6.7,3.));
#21599=CARTESIAN_POINT('Origin',(0.,6.5,3.));
#24874=UNCERTAINTY_MEASURE_WITH_UNIT(LENGTH_MEASURE(0.001),#25101,
'DISTANCE_ACCURACY_VALUE',
'Maximum model space distance between geometric entities at asserted c
onnectivities');
#24979=UNCERTAINTY_MEASURE_WITH_UNIT(LENGTH_MEASURE(0.001),#25101,
'DISTANCE_ACCURACY_VALUE',
'Maximum model space distance between geometric entities at asserted c
onnectivities');
#24995=(
GEOMETRIC_REPRESENTATION_CONTEXT(3)
GLOBAL_UNCERTAINTY_ASSIGNED_CONTEXT((#24874))
GLOBAL_UNIT_ASSIGNED_CONTEXT((#25101,#25103,#25104))
REPRESENTATION_CONTEXT('','3D')
);
#25100=(
GEOMETRIC_REPRESENTATION_CONTEXT(3)
GLOBAL_UNCERTAINTY_ASSIGNED_CONTEXT((#24979))
GLOBAL_UNIT_ASSIGNED_CONTEXT((#25101,#25103,#25104))
REPRESENTATION_CONTEXT('','3D')
);
#25101=(
LENGTH_UNIT()
NAMED_UNIT(*)
SI_UNIT(.CENTI.,.METRE.)
);
#25103=(
NAMED_UNIT(*)
PLANE_ANGLE_UNIT()
SI_UNIT($,.RADIAN.)
);
#25104=(
NAMED_UNIT(*)
SI_UNIT($,.STERADIAN.)
SOLID_ANGLE_UNIT()
);
#25120=SHAPE_DEFINITION_REPRESENTATION(#25240,#25525);
#25240=PRODUCT_DEFINITION_SHAPE('',$,#25646);
#25525=SHAPE_REPRESENTATION('',(#14858),#24995);
#25630=PRODUCT_DEFINITION_CONTEXT('part definition',#25992,'design');
#25646=PRODUCT_DEFINITION('Axle end keeper (1)','Axle end keeper (1)',#25766,
#25630);
#25766=PRODUCT_DEFINITION_FORMATION('',$,#26009);
#25992=APPLICATION_CONTEXT(
'Core Data for Automotive Mechanical Design Process');
#25993=PRODUCT_CONTEXT('part definition',#25992,'mechanical');
#26009=PRODUCT('Axle end keeper (1)','Axle end keeper (1)',
'Axle end keeper (1)',(#25993));
#26185=COLOUR_RGB('Grey',0.48,0.52,0.57);
#26186=FILL_AREA_STYLE_COLOUR('',#26185);
#26187=FILL_AREA_STYLE('',(#26186));
#26188=SURFACE_STYLE_FILL_AREA(#26187);
#26189=SURFACE_SIDE_STYLE('',(#26188));
#26190=SURFACE_STYLE_USAGE(.BOTH.,#26189);
#26191=PRESENTATION_STYLE_ASSIGNMENT((#26190));
ENDSEC;
END-ISO-10303-21;
